ISO-10303-21;
HEADER;
FILE_DESCRIPTION (('STEP AP214'),
    '1' );
FILE_NAME ('hex bolt gradeb_iso_ISO 4015 - M3 x 20 x 12-N.step',
    '2026-10-06T07:34:29',
    ( '' ),
    ( '' ),
    'SwSTEP 2.0',
    'SolidWorks 2025',
    '' );
FILE_SCHEMA (( 'AUTOMOTIVE_DESIGN' ));
ENDSEC;

DATA;
#77=LINE ( 'NONE', #10922, #4868 ) ;
#117=DIRECTION ( 'NONE',  ( 0.000000000000000000, 0.000000000000000000, 1.000000000000000000 ) ) ;
#127=CARTESIAN_POINT ( 'NONE',  ( 0.000000000000000000, -2.381569860407207084, -1.374999999999997113 ) ) ;
#188=PRODUCT_DEFINITION_FORMATION_WITH_SPECIFIED_SOURCE ( 'ANY', '', #10425, .NOT_KNOWN. ) ;
#311=CARTESIAN_POINT ( 'NONE',  ( 21.99999999999999289, 0.000000000000000000, 1.219500000000000028 ) ) ;
#378=CARTESIAN_POINT ( 'NONE',  ( 2.000000000000000000, -1.587713240271461546, 2.750000000000000000 ) ) ;
#385=EDGE_LOOP ( 'NONE', ( #10677, #7810, #419, #2894 ) ) ;
#419=ORIENTED_EDGE ( 'NONE', *, *, #12484, .T. ) ;
#421=DIRECTION ( 'NONE',  ( 1.000000000000000000, 0.000000000000000000, -0.000000000000000000 ) ) ;
#444=ORIENTED_EDGE ( 'NONE', *, *, #9592, .F. ) ;
#456=DIRECTION ( 'NONE',  ( 0.000000000000000000, 0.000000000000000000, -1.000000000000000000 ) ) ;
#503=CARTESIAN_POINT ( 'NONE',  ( 0.000000000000000000, 0.000000000000000000, 0.000000000000000000 ) ) ;
#506=VECTOR ( 'NONE', #7405, 1000.000000000000000 ) ;
#519=CARTESIAN_POINT ( 'NONE',  ( 21.71949999999999648, 0.000000000000000000, 1.500000000000000000 ) ) ;
#522=CARTESIAN_POINT ( 'NONE',  ( 0.2456200930618607225, 1.587713240271468207, -2.750000000000000000 ) ) ;
#528=B_SPLINE_CURVE_WITH_KNOTS ( 'NONE', 3,
 ( #15104, #3195, #13773, #8026, #5416, #11414 ),
 .UNSPECIFIED., .F., .F.,
 ( 4, 2, 4 ),
 ( 0.002949915431443937870, 0.003753579573369721003, 0.004557243715295504136 ),
 .UNSPECIFIED. ) ;
#550=CARTESIAN_POINT ( 'NONE',  ( -1.048203272227196275E-15, -2.516314840832718502, -1.141614847838140490 ) ) ;
#579=CARTESIAN_POINT ( 'NONE',  ( 2.000000000000000000, -3.175426480542940411, 0.000000000000000000 ) ) ;
#630=CARTESIAN_POINT ( 'NONE',  ( 0.02351960456806068828, -2.650883748492876446, -0.9085346626517005753 ) ) ;
#655=CARTESIAN_POINT ( 'NONE',  ( 21.99999999999999289, 0.000000000000000000, 0.000000000000000000 ) ) ;
#723=FACE_OUTER_BOUND ( 'NONE', #9664, .T. ) ;
#732=CARTESIAN_POINT ( 'NONE',  ( 0.2456200930618629430, 3.175426480542944407, 1.454290997841272695E-16 ) ) ;
#799=COLOUR_RGB ( '', 0.66274510, 0.83137255, 0.94901961) ;
#813=CARTESIAN_POINT ( 'NONE',  ( 0.000000000000000000, -7.511572993685817836E-16, 2.749999999999999112 ) ) ;
#866=CARTESIAN_POINT ( 'NONE',  ( 0.000000000000000000, -2.381569860407202643, 1.375000000000004663 ) ) ;
#924=CARTESIAN_POINT ( 'NONE',  ( 0.02351960456805774966, -2.112255972321529285, 1.841465337348299869 ) ) ;
#972=AXIS2_PLACEMENT_3D ( 'NONE', #4604, #14298, #2077 ) ;
#1016=ADVANCED_FACE ( 'NONE', ( #2509 ), #2326, .T. ) ;
#1047=B_SPLINE_CURVE_WITH_KNOTS ( 'NONE', 3,
 ( #2845, #7667, #5054, #3868, #13558, #8927 ),
 .UNSPECIFIED., .F., .F.,
 ( 4, 2, 4 ),
 ( 0.008378281255485226300, 0.009182315005745945308, 0.009986348756006662580 ),
 .UNSPECIFIED. ) ;
#1090=DIRECTION ( 'NONE',  ( 0.000000000000000000, -1.000000000000000000, -2.731481088613025116E-16 ) ) ;
#1113=FACE_OUTER_BOUND ( 'NONE', #15215, .T. ) ;
#1115=EDGE_CURVE ( 'NONE', #10711, #12769, #14133, .T. ) ;
#1192=ORIENTED_EDGE ( 'NONE', *, *, #9834, .F. ) ;
#1207=SURFACE_STYLE_USAGE ( .BOTH. , #2168 ) ;
#1217=ADVANCED_FACE ( 'NONE', ( #2828 ), #7827, .T. ) ;
#1272=AXIS2_PLACEMENT_3D ( 'NONE', #6151, #7263, #117 ) ;
#1273=ADVANCED_FACE ( 'NONE', ( #10242 ), #3060, .F. ) ;
#1299=MECHANICAL_DESIGN_GEOMETRIC_PRESENTATION_REPRESENTATION('',(#2837),#1309);
#1309=( GEOMETRIC_REPRESENTATION_CONTEXT ( 3 ) GLOBAL_UNCERTAINTY_ASSIGNED_CONTEXT ( ( #1691 ) ) GLOBAL_UNIT_ASSIGNED_CONTEXT ( ( #4692, #15567, #9444 ) ) REPRESENTATION_CONTEXT ( 'NONE', 'WORKASPACE' ) );
#1345=CARTESIAN_POINT ( 'NONE',  ( 0.000000000000000000, 0.000000000000000000, 0.000000000000000000 ) ) ;
#1354=VERTEX_POINT ( 'NONE', #2100 ) ;
#1363=ORIENTED_EDGE ( 'NONE', *, *, #5674, .T. ) ;
#1387=CARTESIAN_POINT ( 'NONE',  ( 0.000000000000000000, 0.000000000000000000, 0.000000000000000000 ) ) ;
#1401=DIRECTION ( 'NONE',  ( -0.000000000000000000, 0.4999999999999991118, -0.8660254037844390407 ) ) ;
#1418=DIRECTION ( 'NONE',  ( -1.000000000000000000, -0.000000000000000000, -0.000000000000000000 ) ) ;
#1478=AXIS2_PLACEMENT_3D ( 'NONE', #14443, #7364, #12159 ) ;
#1510=EDGE_LOOP ( 'NONE', ( #2556, #9343, #9484, #11418, #10154 ) ) ;
#1544=FACE_OUTER_BOUND ( 'NONE', #11818, .T. ) ;
#1546=LINE ( 'NONE', #6381, #5145 ) ;
#1623=CARTESIAN_POINT ( 'NONE',  ( 2.000000000000000000, 3.175426480542944407, -3.252606517456511330E-16 ) ) ;
#1650=ORIENTED_EDGE ( 'NONE', *, *, #12484, .F. ) ;
#1691=UNCERTAINTY_MEASURE_WITH_UNIT (LENGTH_MEASURE( 1.000000000000000082E-05 ), #4692, 'distance_accuracy_value', 'NONE');
#1779=CARTESIAN_POINT ( 'NONE',  ( 21.71949999999999648, 1.836970198721030181E-16, -1.500000000000000222 ) ) ;
#1802=FACE_OUTER_BOUND ( 'NONE', #3961, .T. ) ;
#1824=CARTESIAN_POINT ( 'NONE',  ( 0.1708300674639756100, -3.045886356309197573, -0.2243700767916258776 ) ) ;
#1848=CARTESIAN_POINT ( 'NONE',  ( 0.1090894304641079615, 2.915265454974091064, 0.4506121144344771290 ) ) ;
#1889=ORIENTED_EDGE ( 'NONE', *, *, #13553, .F. ) ;
#1896=VECTOR ( 'NONE', #5151, 999.9999999999998863 ) ;
#1991=AXIS2_PLACEMENT_3D ( 'NONE', #12249, #3815, #2554 ) ;
#2011=ORIENTED_EDGE ( 'NONE', *, *, #6190, .T. ) ;
#2038=EDGE_LOOP ( 'NONE', ( #12635, #8168, #11069, #1650 ) ) ;
#2077=DIRECTION ( 'NONE',  ( 0.000000000000000000, -1.000000000000000000, -2.731481088613017720E-16 ) ) ;
#2089=VECTOR ( 'NONE', #1418, 1000.000000000000000 ) ;
#2100=CARTESIAN_POINT ( 'NONE',  ( 0.000000000000000000, 2.381569860407204420, 1.375000000000001110 ) ) ;
#2161=CARTESIAN_POINT ( 'NONE',  ( 0.02311621069196296077, -0.5352285650541119821, -2.750000000000001332 ) ) ;
#2168=SURFACE_SIDE_STYLE ('',( #10866 ) ) ;
#2190=EDGE_CURVE ( 'NONE', #7996, #6134, #5063, .T. ) ;
#2219=DIRECTION ( 'NONE',  ( -1.000000000000000000, -0.000000000000000000, -0.000000000000000000 ) ) ;
#2240=CARTESIAN_POINT ( 'NONE',  ( 0.1709786460663497709, -1.329147683178129924, -2.750000000000000888 ) ) ;
#2241=CONICAL_SURFACE ( 'NONE', #1478, 2.749999999999999112, 1.047197551196600296 ) ;
#2283=DIRECTION ( 'NONE',  ( -0.000000000000000000, 0.000000000000000000, -1.000000000000000000 ) ) ;
#2326=CONICAL_SURFACE ( 'NONE', #13149, 2.749999999999999112, 1.047197551196600296 ) ;
#2362=CARTESIAN_POINT ( 'NONE',  ( 0.1097966057365644815, 1.070857859038820248, 2.750000000000000444 ) ) ;
#2424=EDGE_CURVE ( 'NONE', #3200, #9186, #5461, .T. ) ;
#2439=CARTESIAN_POINT ( 'NONE',  ( 0.09566599640799448856, 2.915698366337650338, -0.4498622899576186773 ) ) ;
#2441=CYLINDRICAL_SURFACE ( 'NONE', #4016, 1.499999999999999778 ) ;
#2473=ADVANCED_FACE ( 'NONE', ( #10661 ), #14580, .F. ) ;
#2496=DIRECTION ( 'NONE',  ( -0.7071067811865425767, 8.659560562354994488E-17, -0.7071067811865525687 ) ) ;
#2509=FACE_OUTER_BOUND ( 'NONE', #7164, .T. ) ;
#2520=CARTESIAN_POINT ( 'NONE',  ( 0.2456200930618618050, 1.587713240271470427, 2.750000000000000888 ) ) ;
#2554=DIRECTION ( 'NONE',  ( 0.000000000000000000, 0.000000000000000000, -1.000000000000000000 ) ) ;
#2556=ORIENTED_EDGE ( 'NONE', *, *, #3184, .F. ) ;
#2565=ADVANCED_FACE ( 'NONE', ( #14272 ), #3467, .F. ) ;
#2583=LINE ( 'NONE', #5895, #10351 ) ;
#2595=CARTESIAN_POINT ( 'NONE',  ( -3.869242359956847046E-15, -2.652070323102386329, 0.9064794551410519929 ) ) ;
#2706=CARTESIAN_POINT ( 'NONE',  ( 21.99999999999999289, 1.665213485140613626E-16, -1.219500000000000028 ) ) ;
#2713=EDGE_LOOP ( 'NONE', ( #4387, #13395, #7759, #13178, #10615 ) ) ;
#2738=AXIS2_PLACEMENT_3D ( 'NONE', #5260, #4304, #9144 ) ;
#2761=CARTESIAN_POINT ( 'NONE',  ( 0.000000000000000000, 2.381569860407203532, -1.375000000000002665 ) ) ;
#2801=CARTESIAN_POINT ( 'NONE',  ( 0.000000000000000000, 0.000000000000000000, 0.000000000000000000 ) ) ;
#2817=PLANE ( 'NONE',  #3939 ) ;
#2828=FACE_OUTER_BOUND ( 'NONE', #8438, .T. ) ;
#2837=STYLED_ITEM ( 'NONE', ( #13045 ), #10736 ) ;
#2844=DIRECTION ( 'NONE',  ( -1.000000000000000000, 0.000000000000000000, -0.000000000000000000 ) ) ;
#2845=CARTESIAN_POINT ( 'NONE',  ( 0.2456200930618607225, 1.587713240271468207, -2.750000000000000000 ) ) ;
#2894=ORIENTED_EDGE ( 'NONE', *, *, #1115, .F. ) ;
#2921=CARTESIAN_POINT ( 'NONE',  ( 0.1090894304641068929, 1.847874265840319330, -2.299387885565524758 ) ) ;
#2922=DIRECTION ( 'NONE',  ( -0.000000000000000000, 0.000000000000000000, 1.000000000000000000 ) ) ;
#2924=EDGE_CURVE ( 'NONE', #7800, #12461, #9498, .T. ) ;
#2928=B_SPLINE_CURVE_WITH_KNOTS ( 'NONE', 3,
 ( #4531, #9359, #15411, #1848, #5722, #732 ),
 .UNSPECIFIED., .F., .F.,
 ( 4, 2, 4 ),
 ( 0.001606744326298686649, 0.002406996759593248332, 0.003207249192887810449 ),
 .UNSPECIFIED. ) ;
#2936=VECTOR ( 'NONE', #10232, 1000.000000000000000 ) ;
#3013=B_SPLINE_CURVE_WITH_KNOTS ( 'NONE', 3,
 ( #14159, #8194, #2161, #6995, #2240, #14699 ),
 .UNSPECIFIED., .F., .F.,
 ( 4, 2, 4 ),
 ( 0.009986348756006662580, 0.01078976120410690340, 0.01159317365220714248 ),
 .UNSPECIFIED. ) ;
#3022=EDGE_LOOP ( 'NONE', ( #13945, #5116, #1889, #5091, #12792 ) ) ;
#3035=ADVANCED_FACE ( 'NONE', ( #13611 ), #2817, .F. ) ;
#3060=PLANE ( 'NONE',  #12582 ) ;
#3084=CARTESIAN_POINT ( 'NONE',  ( 2.000000000000000000, -1.587713240271472648, -2.750000000000000888 ) ) ;
#3122=DIRECTION ( 'NONE',  ( 0.000000000000000000, 0.000000000000000000, 1.000000000000000000 ) ) ;
#3164=EDGE_LOOP ( 'NONE', ( #4569, #10359, #9499 ) ) ;
#3184=EDGE_CURVE ( 'NONE', #5606, #3200, #528, .T. ) ;
#3187=EDGE_CURVE ( 'NONE', #11085, #9186, #12579, .T. ) ;
#3193=ORIENTED_EDGE ( 'NONE', *, *, #13553, .T. ) ;
#3195=CARTESIAN_POINT ( 'NONE',  ( 0.1709786460671990638, -1.329147683181058692, 2.749999999999999556 ) ) ;
#3200=VERTEX_POINT ( 'NONE', #813 ) ;
#3207=ORIENTED_EDGE ( 'NONE', *, *, #3762, .F. ) ;
#3239=ADVANCED_FACE ( 'NONE', ( #6691 ), #10740, .T. ) ;
#3268=ORIENTED_EDGE ( 'NONE', *, *, #13753, .T. ) ;
#3300=DIRECTION ( 'NONE',  ( 1.000000000000000000, 0.000000000000000000, -0.000000000000000000 ) ) ;
#3357=EDGE_CURVE ( 'NONE', #12329, #15368, #3013, .T. ) ;
#3360=ORIENTED_EDGE ( 'NONE', *, *, #3184, .T. ) ;
#3423=PLANE ( 'NONE',  #972 ) ;
#3428=ORIENTED_EDGE ( 'NONE', *, *, #5673, .F. ) ;
#3459=CARTESIAN_POINT ( 'NONE',  ( -3.916680348103880824E-15, -2.246824879981689005, 1.608385152161860621 ) ) ;
#3467=PLANE ( 'NONE',  #14027 ) ;
#3485=CIRCLE ( 'NONE', #2738, 1.219500000000000028 ) ;
#3543=DIRECTION ( 'NONE',  ( 1.000000000000000000, 0.000000000000000000, 0.000000000000000000 ) ) ;
#3560=ORIENTED_EDGE ( 'NONE', *, *, #6190, .F. ) ;
#3599=EDGE_LOOP ( 'NONE', ( #3360, #9569, #3619 ) ) ;
#3601=AXIS2_PLACEMENT_3D ( 'NONE', #1345, #14448, #15543 ) ;
#3617=EDGE_LOOP ( 'NONE', ( #5705, #3268 ) ) ;
#3619=ORIENTED_EDGE ( 'NONE', *, *, #14144, .T. ) ;
#3646=ORIENTED_EDGE ( 'NONE', *, *, #3187, .F. ) ;
#3709=VERTEX_POINT ( 'NONE', #13405 ) ;
#3755=CARTESIAN_POINT ( 'NONE',  ( 2.000000000000000000, -1.587713240271472648, -2.750000000000000888 ) ) ;
#3762=EDGE_CURVE ( 'NONE', #6134, #10091, #8608, .T. ) ;
#3790=AXIS2_PLACEMENT_3D ( 'NONE', #1623, #10008, #8740 ) ;
#3815=DIRECTION ( 'NONE',  ( -1.000000000000000000, -0.000000000000000000, 0.000000000000000000 ) ) ;
#3868=CARTESIAN_POINT ( 'NONE',  ( 0.02377086945385613326, 0.5410735902593410973, -2.749999999999999112 ) ) ;
#3881=DIRECTION ( 'NONE',  ( 0.000000000000000000, 2.731481088613025116E-16, -1.000000000000000000 ) ) ;
#3895=CARTESIAN_POINT ( 'NONE',  ( 0.000000000000000000, 0.000000000000000000, 0.000000000000000000 ) ) ;
#3935=CARTESIAN_POINT ( 'NONE',  ( 0.2456200930617507272, -1.587713240271640958, -2.750000000000000888 ) ) ;
#3939=AXIS2_PLACEMENT_3D ( 'NONE', #8815, #13691, #8739 ) ;
#3961=EDGE_LOOP ( 'NONE', ( #8239, #8863 ) ) ;
#4011=CARTESIAN_POINT ( 'NONE',  ( -1.350735206554858068E-15, 2.246824879981693890, -1.608385152161860399 ) ) ;
#4016=AXIS2_PLACEMENT_3D ( 'NONE', #10978, #4896, #13243 ) ;
#4050=AXIS2_PLACEMENT_3D ( 'NONE', #7134, #2219, #8473 ) ;
#4104=PRODUCT_DEFINITION_SHAPE ( 'NONE', 'NONE',  #12882 ) ;
#4106=DIRECTION ( 'NONE',  ( 0.000000000000000000, 1.000000000000000000, 2.731481088613025116E-16 ) ) ;
#4141=FACE_BOUND ( 'NONE', #3617, .T. ) ;
#4178=ORIENTED_EDGE ( 'NONE', *, *, #14470, .T. ) ;
#4201=ADVANCED_FACE ( 'NONE', ( #10835 ), #2241, .T. ) ;
#4273=CIRCLE ( 'NONE', #11592, 2.749999999999999112 ) ;
#4304=DIRECTION ( 'NONE',  ( -1.000000000000000000, -0.000000000000000000, -0.000000000000000000 ) ) ;
#4317=CARTESIAN_POINT ( 'NONE',  ( 2.000000000000000000, -3.175426480542940411, 0.000000000000000000 ) ) ;
#4342=EDGE_LOOP ( 'NONE', ( #13187, #13739, #3428, #7435, #5061, #8953 ) ) ;
#4377=ORIENTED_EDGE ( 'NONE', *, *, #3357, .F. ) ;
#4387=ORIENTED_EDGE ( 'NONE', *, *, #9139, .F. ) ;
#4429=ADVANCED_FACE ( 'NONE', ( #7196 ), #13578, .T. ) ;
#4473=CARTESIAN_POINT ( 'NONE',  ( 2.000000000000000000, 0.000000000000000000, 0.000000000000000000 ) ) ;
#4530=AXIS2_PLACEMENT_3D ( 'NONE', #2801, #9035, #10141 ) ;
#4531=CARTESIAN_POINT ( 'NONE',  ( 0.000000000000000000, 2.381569860407204420, 1.375000000000001110 ) ) ;
#4568=CARTESIAN_POINT ( 'NONE',  ( 0.000000000000000000, 0.000000000000000000, 0.000000000000000000 ) ) ;
#4569=ORIENTED_EDGE ( 'NONE', *, *, #6717, .T. ) ;
#4577=EDGE_LOOP ( 'NONE', ( #14153, #4824, #7591, #6985 ) ) ;
#4598=AXIS2_PLACEMENT_3D ( 'NONE', #6254, #7681, #456 ) ;
#4604=CARTESIAN_POINT ( 'NONE',  ( 2.000000000000000000, 1.587713240271468207, -2.750000000000000000 ) ) ;
#4652=B_SPLINE_CURVE_WITH_KNOTS ( 'NONE', 3,
 ( #13311, #9336, #2595, #866 ),
 .UNSPECIFIED., .F., .F.,
 ( 4, 4 ),
 ( 2.380742992393109920E-07, 0.001606744326298693154 ),
 .UNSPECIFIED. ) ;
#4692=( LENGTH_UNIT ( ) NAMED_UNIT ( * ) SI_UNIT ( .MILLI., .METRE. ) );
#4717=CARTESIAN_POINT ( 'NONE',  ( 0.000000000000000000, -2.381569860407202643, 1.375000000000004663 ) ) ;
#4794=DIRECTION ( 'NONE',  ( -1.000000000000000000, -0.000000000000000000, -0.000000000000000000 ) ) ;
#4824=ORIENTED_EDGE ( 'NONE', *, *, #1115, .T. ) ;
#4868=VECTOR ( 'NONE', #9732, 1000.000000000000000 ) ;
#4896=DIRECTION ( 'NONE',  ( -1.000000000000000000, -0.000000000000000000, -0.000000000000000000 ) ) ;
#4933=VERTEX_POINT ( 'NONE', #14963 ) ;
#4965=CARTESIAN_POINT ( 'NONE',  ( 0.000000000000000000, 1.836970198721029688E-16, -1.499999999999999778 ) ) ;
#5044=CARTESIAN_POINT ( 'NONE',  ( 0.000000000000000000, 2.381569860407203532, -1.375000000000002665 ) ) ;
#5054=CARTESIAN_POINT ( 'NONE',  ( 0.1097966057364734849, 1.070857859039281657, -2.750000000000000444 ) ) ;
#5061=ORIENTED_EDGE ( 'NONE', *, *, #9834, .T. ) ;
#5063=LINE ( 'NONE', #12540, #11118 ) ;
#5091=ORIENTED_EDGE ( 'NONE', *, *, #5142, .T. ) ;
#5116=ORIENTED_EDGE ( 'NONE', *, *, #7868, .F. ) ;
#5122=CARTESIAN_POINT ( 'NONE',  ( 0.2456200930618629430, 3.175426480542944407, 1.454290997841272695E-16 ) ) ;
#5135=ORIENTED_EDGE ( 'NONE', *, *, #10489, .T. ) ;
#5142=EDGE_CURVE ( 'NONE', #8109, #13181, #12237, .T. ) ;
#5145=VECTOR ( 'NONE', #10010, 999.9999999999998863 ) ;
#5151=DIRECTION ( 'NONE',  ( -0.7071067811865425767, 0.000000000000000000, 0.7071067811865525687 ) ) ;
#5178=EDGE_CURVE ( 'NONE', #7996, #5606, #6654, .T. ) ;
#5192=AXIS2_PLACEMENT_3D ( 'NONE', #655, #5495, #3122 ) ;
#5213=AXIS2_PLACEMENT_3D ( 'NONE', #9549, #14349, #2283 ) ;
#5241=CARTESIAN_POINT ( 'NONE',  ( 2.000000000000000000, 0.000000000000000000, 1.499999999999999778 ) ) ;
#5251=( GEOMETRIC_REPRESENTATION_CONTEXT ( 3 ) GLOBAL_UNCERTAINTY_ASSIGNED_CONTEXT ( ( #9162 ) ) GLOBAL_UNIT_ASSIGNED_CONTEXT ( ( #9211, #8032, #9442 ) ) REPRESENTATION_CONTEXT ( 'NONE', 'WORKASPACE' ) );
#5260=CARTESIAN_POINT ( 'NONE',  ( 21.99999999999999289, 0.000000000000000000, 0.000000000000000000 ) ) ;
#5300=EDGE_LOOP ( 'NONE', ( #14149, #444, #3207, #6306, #12153 ) ) ;
#5344=DIRECTION ( 'NONE',  ( 1.000000000000000000, 0.000000000000000000, 0.000000000000000000 ) ) ;
#5416=CARTESIAN_POINT ( 'NONE',  ( 7.165898733771380869E-16, -0.2686526913948933948, 2.750000000000000888 ) ) ;
#5452=VECTOR ( 'NONE', #6639, 1000.000000000000000 ) ;
#5461=B_SPLINE_CURVE_WITH_KNOTS ( 'NONE', 3,
 ( #10424, #10900, #13163, #2362, #7271, #2520 ),
 .UNSPECIFIED., .F., .F.,
 ( 4, 2, 4 ),
 ( 0.004557243715295504136, 0.005361529354039402256, 0.006165814992783300377 ),
 .UNSPECIFIED. ) ;
#5482=EDGE_CURVE ( 'NONE', #9708, #7691, #5568, .T. ) ;
#5495=DIRECTION ( 'NONE',  ( -1.000000000000000000, -0.000000000000000000, -0.000000000000000000 ) ) ;
#5508=ADVANCED_FACE ( 'NONE', ( #7270 ), #14502, .T. ) ;
#5550=ADVANCED_FACE ( 'NONE', ( #9071 ), #9946, .F. ) ;
#5568=B_SPLINE_CURVE_WITH_KNOTS ( 'NONE', 3,
 ( #5122, #2439, #12220, #5044 ),
 .UNSPECIFIED., .F., .F.,
 ( 4, 4 ),
 ( 2.380742992386844787E-07, 0.001606744326298692937 ),
 .UNSPECIFIED. ) ;
#5571=ORIENTED_EDGE ( 'NONE', *, *, #12235, .F. ) ;
#5606=VERTEX_POINT ( 'NONE', #8918 ) ;
#5669=DIRECTION ( 'NONE',  ( 0.000000000000000000, -0.5000000000000006661, 0.8660254037844382635 ) ) ;
#5673=EDGE_CURVE ( 'NONE', #4933, #12236, #12430, .T. ) ;
#5674=EDGE_CURVE ( 'NONE', #6130, #11085, #7012, .T. ) ;
#5681=DIRECTION ( 'NONE',  ( 1.000000000000000000, 0.000000000000000000, 0.000000000000000000 ) ) ;
#5705=ORIENTED_EDGE ( 'NONE', *, *, #15207, .T. ) ;
#5722=CARTESIAN_POINT ( 'NONE',  ( 0.1708300674639772754, 3.045886356309201126, 0.2243700767916273764 ) ) ;
#5742=CARTESIAN_POINT ( 'NONE',  ( 0.000000000000000000, 0.000000000000000000, 0.000000000000000000 ) ) ;
#5747=CARTESIAN_POINT ( 'NONE',  ( 0.2456200930618607225, 1.587713240271468207, -2.750000000000000000 ) ) ;
#5826=AXIS2_PLACEMENT_3D ( 'NONE', #3895, #7618, #6431 ) ;
#5895=CARTESIAN_POINT ( 'NONE',  ( 21.99999999999999289, 1.493456771560197319E-16, -1.219500000000000028 ) ) ;
#5902=FACE_OUTER_BOUND ( 'NONE', #385, .T. ) ;
#5943=CARTESIAN_POINT ( 'NONE',  ( 0.000000000000000000, -2.381569860407207084, -1.374999999999997113 ) ) ;
#5958=LINE ( 'NONE', #13515, #10837 ) ;
#5959=AXIS2_PLACEMENT_3D ( 'NONE', #7013, #10639, #15432 ) ;
#5962=FILL_AREA_STYLE_COLOUR ( '', #799 ) ;
#6032=ORIENTED_EDGE ( 'NONE', *, *, #10886, .T. ) ;
#6076=DIRECTION ( 'NONE',  ( 0.000000000000000000, 0.000000000000000000, -1.000000000000000000 ) ) ;
#6130=VERTEX_POINT ( 'NONE', #6611 ) ;
#6134=VERTEX_POINT ( 'NONE', #579 ) ;
#6151=CARTESIAN_POINT ( 'NONE',  ( 21.71949999999999648, 0.000000000000000000, 0.000000000000000000 ) ) ;
#6190=EDGE_CURVE ( 'NONE', #1354, #9708, #2928, .T. ) ;
#6254=CARTESIAN_POINT ( 'NONE',  ( 0.000000000000000000, 0.000000000000000000, 0.000000000000000000 ) ) ;
#6306=ORIENTED_EDGE ( 'NONE', *, *, #12820, .T. ) ;
#6343=CARTESIAN_POINT ( 'NONE',  ( 2.000000000000000000, 1.587713240271470427, 2.750000000000000888 ) ) ;
#6380=PLANE ( 'NONE',  #3790 ) ;
#6381=CARTESIAN_POINT ( 'NONE',  ( 2.000000000000000000, 1.587713240271468207, -2.750000000000000000 ) ) ;
#6431=DIRECTION ( 'NONE',  ( 0.000000000000000000, 0.000000000000000000, -1.000000000000000000 ) ) ;
#6460=CARTESIAN_POINT ( 'NONE',  ( 0.2456200930618618050, 1.587713240271470427, 2.750000000000000888 ) ) ;
#6473=DIRECTION ( 'NONE',  ( 0.000000000000000000, -0.4999999999999991118, 0.8660254037844390407 ) ) ;
#6482=PRODUCT_DEFINITION_CONTEXT ( 'detailed design', #9991, 'design' ) ;
#6519=DIRECTION ( 'NONE',  ( 0.000000000000000000, 0.000000000000000000, -1.000000000000000000 ) ) ;
#6533=CIRCLE ( 'NONE', #12062, 2.749999999999999112 ) ;
#6538=ORIENTED_EDGE ( 'NONE', *, *, #9592, .T. ) ;
#6549=ORIENTED_EDGE ( 'NONE', *, *, #11530, .T. ) ;
#6574=DIRECTION ( 'NONE',  ( -0.000000000000000000, -0.5000000000000018874, -0.8660254037844375974 ) ) ;
#6609=B_SPLINE_CURVE_WITH_KNOTS ( 'NONE', 3,
 ( #6460, #11115, #11191, #7483 ),
 .UNSPECIFIED., .F., .F.,
 ( 4, 4 ),
 ( 2.380742992386783113E-07, 0.001606744326298686649 ),
 .UNSPECIFIED. ) ;
#6611=CARTESIAN_POINT ( 'NONE',  ( 2.000000000000000000, 3.175426480542944407, 0.000000000000000000 ) ) ;
#6639=DIRECTION ( 'NONE',  ( -1.000000000000000000, -0.000000000000000000, -0.000000000000000000 ) ) ;
#6654=LINE ( 'NONE', #13730, #12206 ) ;
#6691=FACE_OUTER_BOUND ( 'NONE', #2038, .T. ) ;
#6701=DIRECTION ( 'NONE',  ( 0.000000000000000000, -0.8660254037844380415, 0.5000000000000012212 ) ) ;
#6717=EDGE_CURVE ( 'NONE', #15368, #12236, #14563, .T. ) ;
#6735=EDGE_LOOP ( 'NONE', ( #11120, #3646, #13717, #12166, #3560 ) ) ;
#6779=CARTESIAN_POINT ( 'NONE',  ( 2.000000000000000000, 3.175426480542944407, 0.000000000000000000 ) ) ;
#6825=CARTESIAN_POINT ( 'NONE',  ( 21.99999999999999289, 0.000000000000000000, 1.219500000000000028 ) ) ;
#6885=ADVANCED_FACE ( 'NONE', ( #7428 ), #2441, .T. ) ;
#6985=ORIENTED_EDGE ( 'NONE', *, *, #13753, .F. ) ;
#6995=CARTESIAN_POINT ( 'NONE',  ( 0.1085346982753684214, -1.064859738956084545, -2.750000000000000444 ) ) ;
#7012=LINE ( 'NONE', #6779, #13689 ) ;
#7013=CARTESIAN_POINT ( 'NONE',  ( 21.99999999999999289, 0.000000000000000000, 0.000000000000000000 ) ) ;
#7026=CARTESIAN_POINT ( 'NONE',  ( 0.1708300674639733063, -1.717253364505205271, 2.525629923208374539 ) ) ;
#7068=ORIENTED_EDGE ( 'NONE', *, *, #10427, .T. ) ;
#7089=LINE ( 'NONE', #3755, #506 ) ;
#7129=ADVANCED_FACE ( 'NONE', ( #4141, #1544 ), #6380, .T. ) ;
#7134=CARTESIAN_POINT ( 'NONE',  ( 0.000000000000000000, 0.000000000000000000, 0.000000000000000000 ) ) ;
#7164=EDGE_LOOP ( 'NONE', ( #15135, #6549, #1192 ) ) ;
#7196=FACE_OUTER_BOUND ( 'NONE', #3599, .T. ) ;
#7263=DIRECTION ( 'NONE',  ( -1.000000000000000000, -0.000000000000000000, -0.000000000000000000 ) ) ;
#7270=FACE_OUTER_BOUND ( 'NONE', #7402, .T. ) ;
#7271=CARTESIAN_POINT ( 'NONE',  ( 0.1714848819421568860, 1.330901335693120302, 2.750000000000000888 ) ) ;
#7329=ORIENTED_EDGE ( 'NONE', *, *, #2190, .T. ) ;
#7348=DIRECTION ( 'NONE',  ( 0.000000000000000000, 0.000000000000000000, -1.000000000000000000 ) ) ;
#7351=DIRECTION ( 'NONE',  ( 0.000000000000000000, 0.000000000000000000, 1.000000000000000000 ) ) ;
#7364=DIRECTION ( 'NONE',  ( 1.000000000000000000, 0.000000000000000000, 0.000000000000000000 ) ) ;
#7402=EDGE_LOOP ( 'NONE', ( #12447, #7068, #15328, #12018 ) ) ;
#7405=DIRECTION ( 'NONE',  ( -1.000000000000000000, -0.000000000000000000, -0.000000000000000000 ) ) ;
#7428=FACE_OUTER_BOUND ( 'NONE', #4577, .T. ) ;
#7429=CARTESIAN_POINT ( 'NONE',  ( 2.000000000000000000, -1.587713240271472648, -2.750000000000000888 ) ) ;
#7435=ORIENTED_EDGE ( 'NONE', *, *, #9636, .F. ) ;
#7483=CARTESIAN_POINT ( 'NONE',  ( 0.000000000000000000, 2.381569860407204420, 1.375000000000001110 ) ) ;
#7496=APPLICATION_CONTEXT ( 'automotive_design' ) ;
#7513=EDGE_CURVE ( 'NONE', #12769, #11977, #5958, .T. ) ;
#7587=EDGE_CURVE ( 'NONE', #12236, #12329, #11340, .T. ) ;
#7591=ORIENTED_EDGE ( 'NONE', *, *, #7513, .T. ) ;
#7618=DIRECTION ( 'NONE',  ( 1.000000000000000000, 0.000000000000000000, -0.000000000000000000 ) ) ;
#7653=ORIENTED_EDGE ( 'NONE', *, *, #9139, .T. ) ;
#7657=DIRECTION ( 'NONE',  ( -0.000000000000000000, 0.8660254037844391517, 0.4999999999999991673 ) ) ;
#7667=CARTESIAN_POINT ( 'NONE',  ( 0.1714848819424952819, 1.330901335694294030, -2.749999999999999556 ) ) ;
#7681=DIRECTION ( 'NONE',  ( 1.000000000000000000, 0.000000000000000000, 0.000000000000000000 ) ) ;
#7691=VERTEX_POINT ( 'NONE', #13594 ) ;
#7759=ORIENTED_EDGE ( 'NONE', *, *, #2190, .F. ) ;
#7763=DIRECTION ( 'NONE',  ( 0.000000000000000000, 0.000000000000000000, 1.000000000000000000 ) ) ;
#7800=VERTEX_POINT ( 'NONE', #6825 ) ;
#7807=CARTESIAN_POINT ( 'NONE',  ( 0.000000000000000000, 0.000000000000000000, 0.000000000000000000 ) ) ;
#7810=ORIENTED_EDGE ( 'NONE', *, *, #14425, .T. ) ;
#7817=CARTESIAN_POINT ( 'NONE',  ( 2.000000000000000000, -1.587713240271472648, -2.750000000000000888 ) ) ;
#7827=CONICAL_SURFACE ( 'NONE', #14100, 2.749999999999999112, 1.047197551196600296 ) ;
#7868=EDGE_CURVE ( 'NONE', #6130, #9708, #77, .T. ) ;
#7904=CLOSED_SHELL ( 'NONE', ( #3239, #5508, #1273, #2565, #8100, #3035, #5550, #15025, #7129, #6885, #12985, #13603, #8014, #1217, #4429, #1016, #7931, #4201, #2473 ) ) ;
#7914=DIRECTION ( 'NONE',  ( -1.000000000000000000, -0.000000000000000000, -0.000000000000000000 ) ) ;
#7931=ADVANCED_FACE ( 'NONE', ( #1113 ), #9405, .T. ) ;
#7996=VERTEX_POINT ( 'NONE', #378 ) ;
#8014=ADVANCED_FACE ( 'NONE', ( #11294 ), #15424, .T. ) ;
#8026=CARTESIAN_POINT ( 'NONE',  ( 0.02311621069251519611, -0.5352285650591098731, 2.749999999999999112 ) ) ;
#8032=( NAMED_UNIT ( * ) PLANE_ANGLE_UNIT ( ) SI_UNIT ( $, .RADIAN. ) );
#8100=ADVANCED_FACE ( 'NONE', ( #8862 ), #13650, .F. ) ;
#8109=VERTEX_POINT ( 'NONE', #12543 ) ;
#8147=DIRECTION ( 'NONE',  ( 0.000000000000000000, 0.000000000000000000, 1.000000000000000000 ) ) ;
#8168=ORIENTED_EDGE ( 'NONE', *, *, #8647, .T. ) ;
#8194=CARTESIAN_POINT ( 'NONE',  ( 7.375539388216818230E-16, -0.2686526913914984438, -2.750000000000000888 ) ) ;
#8239=ORIENTED_EDGE ( 'NONE', *, *, #2924, .F. ) ;
#8306=VECTOR ( 'NONE', #1401, 1000.000000000000114 ) ;
#8348=PRODUCT_CONTEXT ( 'NONE', #7496, 'mechanical' ) ;
#8369=CIRCLE ( 'NONE', #5826, 2.749999999999999112 ) ;
#8399=ORIENTED_EDGE ( 'NONE', *, *, #5673, .T. ) ;
#8438=EDGE_LOOP ( 'NONE', ( #7653, #8399, #11485 ) ) ;
#8473=DIRECTION ( 'NONE',  ( 0.000000000000000000, 0.000000000000000000, 1.000000000000000000 ) ) ;
#8555=CARTESIAN_POINT ( 'NONE',  ( 0.000000000000000000, 7.511572993685799101E-16, -2.750000000000000444 ) ) ;
#8608=LINE ( 'NONE', #7429, #8306 ) ;
#8647=EDGE_CURVE ( 'NONE', #12461, #10711, #2583, .T. ) ;
#8684=DIRECTION ( 'NONE',  ( -1.000000000000000000, -0.000000000000000000, -0.000000000000000000 ) ) ;
#8739=DIRECTION ( 'NONE',  ( 0.000000000000000000, 0.5000000000000018874, 0.8660254037844375974 ) ) ;
#8740=DIRECTION ( 'NONE',  ( -0.000000000000000000, 0.000000000000000000, -1.000000000000000000 ) ) ;
#8813=CIRCLE ( 'NONE', #1991, 1.499999999999999778 ) ;
#8815=CARTESIAN_POINT ( 'NONE',  ( 2.000000000000000000, -3.175426480542940411, 0.000000000000000000 ) ) ;
#8842=CARTESIAN_POINT ( 'NONE',  ( 0.1708300674639753880, 1.717253364505211266, -2.525629923208373651 ) ) ;
#8862=FACE_OUTER_BOUND ( 'NONE', #1510, .T. ) ;
#8863=ORIENTED_EDGE ( 'NONE', *, *, #14425, .F. ) ;
#8909=DIRECTION ( 'NONE',  ( 0.000000000000000000, 0.000000000000000000, -1.000000000000000000 ) ) ;
#8918=CARTESIAN_POINT ( 'NONE',  ( 0.2456200930618588907, -1.587713240271461546, 2.750000000000000000 ) ) ;
#8925=CARTESIAN_POINT ( 'NONE',  ( 0.02351960456806058766, 2.112255972321535502, -1.841465337348300535 ) ) ;
#8927=CARTESIAN_POINT ( 'NONE',  ( 0.000000000000000000, 7.511572993685799101E-16, -2.750000000000000444 ) ) ;
#8953=ORIENTED_EDGE ( 'NONE', *, *, #10886, .F. ) ;
#8955=CARTESIAN_POINT ( 'NONE',  ( 0.2456200930618629430, 3.175426480542944407, 1.454290997841272695E-16 ) ) ;
#9023=CARTESIAN_POINT ( 'NONE',  ( 21.71949999999999648, 0.000000000000000000, 0.000000000000000000 ) ) ;
#9035=DIRECTION ( 'NONE',  ( 1.000000000000000000, 0.000000000000000000, -0.000000000000000000 ) ) ;
#9071=FACE_OUTER_BOUND ( 'NONE', #5300, .T. ) ;
#9136=SHAPE_REPRESENTATION_RELATIONSHIP ( 'NONE' , 'NONE' ,  #11876, #9237 ) ;
#9139=EDGE_CURVE ( 'NONE', #9639, #4933, #4652, .T. ) ;
#9144=DIRECTION ( 'NONE',  ( 0.000000000000000000, 0.000000000000000000, 1.000000000000000000 ) ) ;
#9162=UNCERTAINTY_MEASURE_WITH_UNIT (LENGTH_MEASURE( 1.000000000000000082E-05 ), #9211, 'distance_accuracy_value', 'NONE');
#9186=VERTEX_POINT ( 'NONE', #13783 ) ;
#9211=( LENGTH_UNIT ( ) NAMED_UNIT ( * ) SI_UNIT ( .MILLI., .METRE. ) );
#9237=ADVANCED_BREP_SHAPE_REPRESENTATION ( '', ( #10736, #12337 ), #5251 ) ;
#9251=B_SPLINE_CURVE_WITH_KNOTS ( 'NONE', 3,
 ( #2761, #4011, #8925, #2921, #8842, #522 ),
 .UNSPECIFIED., .F., .F.,
 ( 4, 2, 4 ),
 ( 0.001606744326298692937, 0.002406996759593252235, 0.003207249192887811316 ),
 .UNSPECIFIED. ) ;
#9336=CARTESIAN_POINT ( 'NONE',  ( 0.09566599640799207382, -2.915698366337646341, 0.4498622899576191214 ) ) ;
#9343=ORIENTED_EDGE ( 'NONE', *, *, #5178, .F. ) ;
#9351=LINE ( 'NONE', #10765, #12478 ) ;
#9359=CARTESIAN_POINT ( 'NONE',  ( -4.116580123655898169E-16, 2.516314840832717170, 1.141614847838143820 ) ) ;
#9405=CONICAL_SURFACE ( 'NONE', #3601, 2.749999999999999112, 1.047197551196600296 ) ;
#9442=( NAMED_UNIT ( * ) SI_UNIT ( $, .STERADIAN. ) SOLID_ANGLE_UNIT ( ) );
#9444=( NAMED_UNIT ( * ) SI_UNIT ( $, .STERADIAN. ) SOLID_ANGLE_UNIT ( ) );
#9484=ORIENTED_EDGE ( 'NONE', *, *, #10269, .F. ) ;
#9498=CIRCLE ( 'NONE', #5959, 1.219500000000000028 ) ;
#9499=ORIENTED_EDGE ( 'NONE', *, *, #3357, .T. ) ;
#9539=CARTESIAN_POINT ( 'NONE',  ( 0.1090894304641042839, -1.847874265840313335, 2.299387885565523870 ) ) ;
#9549=CARTESIAN_POINT ( 'NONE',  ( 0.000000000000000000, 3.175426480542944407, -3.252606517456511330E-16 ) ) ;
#9569=ORIENTED_EDGE ( 'NONE', *, *, #9636, .T. ) ;
#9592=EDGE_CURVE ( 'NONE', #10091, #15368, #7089, .T. ) ;
#9596=SHAPE_DEFINITION_REPRESENTATION ( #4104, #11876 ) ;
#9598=FILL_AREA_STYLE ('',( #5962 ) ) ;
#9636=EDGE_CURVE ( 'NONE', #3200, #4933, #8369, .T. ) ;
#9639=VERTEX_POINT ( 'NONE', #13355 ) ;
#9664=EDGE_LOOP ( 'NONE', ( #14200, #12726, #5571, #6538, #4377 ) ) ;
#9704=DIRECTION ( 'NONE',  ( 1.000000000000000000, 0.000000000000000000, 0.000000000000000000 ) ) ;
#9708=VERTEX_POINT ( 'NONE', #8955 ) ;
#9732=DIRECTION ( 'NONE',  ( -1.000000000000000000, -0.000000000000000000, -0.000000000000000000 ) ) ;
#9834=EDGE_CURVE ( 'NONE', #3200, #1354, #10881, .T. ) ;
#9871=CARTESIAN_POINT ( 'NONE',  ( 0.000000000000000000, 0.000000000000000000, 0.000000000000000000 ) ) ;
#9872=CARTESIAN_POINT ( 'NONE',  ( 2.000000000000000000, 3.175426480542944407, 0.000000000000000000 ) ) ;
#9935=AXIS2_PLACEMENT_3D ( 'NONE', #5742, #3300, #12992 ) ;
#9946=PLANE ( 'NONE',  #14197 ) ;
#9990=CIRCLE ( 'NONE', #11493, 1.500000000000000000 ) ;
#9991=APPLICATION_CONTEXT ( 'automotive_design' ) ;
#10008=DIRECTION ( 'NONE',  ( 1.000000000000000000, 0.000000000000000000, -0.000000000000000000 ) ) ;
#10010=DIRECTION ( 'NONE',  ( 0.000000000000000000, 0.5000000000000012212, 0.8660254037844380415 ) ) ;
#10091=VERTEX_POINT ( 'NONE', #3084 ) ;
#10104=CARTESIAN_POINT ( 'NONE',  ( 21.99999999999999289, 0.000000000000000000, 0.000000000000000000 ) ) ;
#10141=DIRECTION ( 'NONE',  ( 0.000000000000000000, 0.000000000000000000, -1.000000000000000000 ) ) ;
#10154=ORIENTED_EDGE ( 'NONE', *, *, #2424, .F. ) ;
#10208=CARTESIAN_POINT ( 'NONE',  ( 0.2456200930618607225, -3.175426480542939967, 2.004439700231694701E-16 ) ) ;
#10232=DIRECTION ( 'NONE',  ( -1.000000000000000000, -0.000000000000000000, -0.000000000000000000 ) ) ;
#10242=FACE_OUTER_BOUND ( 'NONE', #3022, .T. ) ;
#10269=EDGE_CURVE ( 'NONE', #11085, #7996, #11916, .T. ) ;
#10278=CARTESIAN_POINT ( 'NONE',  ( 0.2456200930617507272, -1.587713240271640958, -2.750000000000000888 ) ) ;
#10351=VECTOR ( 'NONE', #2496, 999.9999999999998863 ) ;
#10359=ORIENTED_EDGE ( 'NONE', *, *, #7587, .T. ) ;
#10372=DIRECTION ( 'NONE',  ( 1.000000000000000000, 0.000000000000000000, -0.000000000000000000 ) ) ;
#10385=CARTESIAN_POINT ( 'NONE',  ( 2.000000000000000000, 1.587713240271470427, 2.750000000000000888 ) ) ;
#10424=CARTESIAN_POINT ( 'NONE',  ( 0.000000000000000000, -7.511572993685817836E-16, 2.749999999999999112 ) ) ;
#10425=PRODUCT ( 'hex bolt gradeb_iso_ISO 4015 - M3 x 20 x 12-N', 'hex bolt gradeb_iso_ISO 4015 - M3 x 20 x 12-N', '', ( #8348 ) ) ;
#10427=EDGE_CURVE ( 'NONE', #10711, #3709, #13399, .T. ) ;
#10489=EDGE_CURVE ( 'NONE', #13181, #12329, #1047, .T. ) ;
#10611=DIRECTION ( 'NONE',  ( -0.000000000000000000, 1.000000000000000000, 2.731481088613017720E-16 ) ) ;
#10615=ORIENTED_EDGE ( 'NONE', *, *, #14144, .F. ) ;
#10639=DIRECTION ( 'NONE',  ( -1.000000000000000000, -0.000000000000000000, -0.000000000000000000 ) ) ;
#10647=DIRECTION ( 'NONE',  ( 0.000000000000000000, 0.000000000000000000, -1.000000000000000000 ) ) ;
#10661=FACE_OUTER_BOUND ( 'NONE', #4342, .T. ) ;
#10677=ORIENTED_EDGE ( 'NONE', *, *, #8647, .F. ) ;
#10685=ORIENTED_EDGE ( 'NONE', *, *, #12235, .T. ) ;
#10711=VERTEX_POINT ( 'NONE', #1779 ) ;
#10736=MANIFOLD_SOLID_BREP ( 'HeadChamfer', #7904 ) ;
#10740=CONICAL_SURFACE ( 'NONE', #5192, 1.219500000000000028, 0.7853981633974552734 ) ;
#10765=CARTESIAN_POINT ( 'NONE',  ( 2.000000000000000000, 1.587713240271468207, -2.750000000000000000 ) ) ;
#10801=AXIS2_PLACEMENT_3D ( 'NONE', #4473, #14337, #10647 ) ;
#10815=CARTESIAN_POINT ( 'NONE',  ( 2.000000000000000000, 1.587713240271470427, 2.750000000000000888 ) ) ;
#10835=FACE_OUTER_BOUND ( 'NONE', #15075, .T. ) ;
#10837=VECTOR ( 'NONE', #13833, 1000.000000000000000 ) ;
#10851=CARTESIAN_POINT ( 'NONE',  ( 0.000000000000000000, -2.381569860407207084, -1.374999999999997113 ) ) ;
#10866=SURFACE_STYLE_FILL_AREA ( #9598 ) ;
#10881=CIRCLE ( 'NONE', #4050, 2.749999999999999112 ) ;
#10886=EDGE_CURVE ( 'NONE', #7691, #1354, #4273, .T. ) ;
#10897=CARTESIAN_POINT ( 'NONE',  ( 0.000000000000000000, 0.000000000000000000, 0.000000000000000000 ) ) ;
#10900=CARTESIAN_POINT ( 'NONE',  ( 7.890111903673804700E-16, 0.2688604483224075747, 2.750000000000000888 ) ) ;
#10922=CARTESIAN_POINT ( 'NONE',  ( 2.000000000000000000, 3.175426480542944407, 0.000000000000000000 ) ) ;
#10978=CARTESIAN_POINT ( 'NONE',  ( 0.000000000000000000, 0.000000000000000000, 0.000000000000000000 ) ) ;
#11046=DIRECTION ( 'NONE',  ( 0.000000000000000000, -0.8660254037844382635, -0.5000000000000006661 ) ) ;
#11069=ORIENTED_EDGE ( 'NONE', *, *, #12648, .F. ) ;
#11085=VERTEX_POINT ( 'NONE', #6343 ) ;
#11115=CARTESIAN_POINT ( 'NONE',  ( 0.09566599640799457183, 1.847441354476763165, 2.300137710042383432 ) ) ;
#11118=VECTOR ( 'NONE', #6574, 1000.000000000000000 ) ;
#11120=ORIENTED_EDGE ( 'NONE', *, *, #11530, .F. ) ;
#11131=CARTESIAN_POINT ( 'NONE',  ( -9.724672249307026221E-16, -2.111069397712039830, -1.843520544858919807 ) ) ;
#11158=LINE ( 'NONE', #311, #1896 ) ;
#11191=CARTESIAN_POINT ( 'NONE',  ( -3.638415890883090848E-16, 2.111069397712021178, 1.843520544858951560 ) ) ;
#11204=DIRECTION ( 'NONE',  ( 0.000000000000000000, 0.5000000000000006661, -0.8660254037844382635 ) ) ;
#11233=CARTESIAN_POINT ( 'NONE',  ( 0.1090894304641069068, -2.915265454974089732, -0.4506121144344751306 ) ) ;
#11294=FACE_OUTER_BOUND ( 'NONE', #3164, .T. ) ;
#11340=CIRCLE ( 'NONE', #4530, 2.749999999999999112 ) ;
#11364=PLANE ( 'NONE',  #11698 ) ;
#11399=VECTOR ( 'NONE', #13238, 1000.000000000000000 ) ;
#11414=CARTESIAN_POINT ( 'NONE',  ( 0.000000000000000000, -7.511572993685817836E-16, 2.749999999999999112 ) ) ;
#11418=ORIENTED_EDGE ( 'NONE', *, *, #3187, .T. ) ;
#11425=AXIS2_PLACEMENT_3D ( 'NONE', #9871, #8684, #7351 ) ;
#11485=ORIENTED_EDGE ( 'NONE', *, *, #15322, .T. ) ;
#11493=AXIS2_PLACEMENT_3D ( 'NONE', #9023, #13740, #7763 ) ;
#11530=EDGE_CURVE ( 'NONE', #9186, #1354, #6609, .T. ) ;
#11554=CARTESIAN_POINT ( 'NONE',  ( 0.000000000000000000, 0.000000000000000000, 0.000000000000000000 ) ) ;
#11592=AXIS2_PLACEMENT_3D ( 'NONE', #11554, #10372, #6519 ) ;
#11698=AXIS2_PLACEMENT_3D ( 'NONE', #10104, #2844, #2922 ) ;
#11818=EDGE_LOOP ( 'NONE', ( #3193, #1363, #13542, #7329, #13365, #10685 ) ) ;
#11876=SHAPE_REPRESENTATION ( 'hex bolt gradeb_iso_ISO 4015 - M3 x 20 x 12-N', ( #12337 ), #5251 ) ;
#11916=LINE ( 'NONE', #10815, #14403 ) ;
#11977=VERTEX_POINT ( 'NONE', #5241 ) ;
#12018=ORIENTED_EDGE ( 'NONE', *, *, #7513, .F. ) ;
#12062=AXIS2_PLACEMENT_3D ( 'NONE', #7807, #421, #14956 ) ;
#12153=ORIENTED_EDGE ( 'NONE', *, *, #15322, .F. ) ;
#12159=DIRECTION ( 'NONE',  ( 0.000000000000000000, 0.000000000000000000, -1.000000000000000000 ) ) ;
#12166=ORIENTED_EDGE ( 'NONE', *, *, #7868, .T. ) ;
#12180=AXIS2_PLACEMENT_3D ( 'NONE', #14179, #4794, #15356 ) ;
#12206=VECTOR ( 'NONE', #7914, 1000.000000000000000 ) ;
#12220=CARTESIAN_POINT ( 'NONE',  ( -1.302788261070087384E-15, 2.652070323102390770, -0.9064794551410521040 ) ) ;
#12222=CARTESIAN_POINT ( 'NONE',  ( 0.09566599640798266468, -1.847441354476797359, -2.300137710042325256 ) ) ;
#12235=EDGE_CURVE ( 'NONE', #10091, #8109, #9351, .T. ) ;
#12236=VERTEX_POINT ( 'NONE', #5943 ) ;
#12237=LINE ( 'NONE', #14679, #2089 ) ;
#12249=CARTESIAN_POINT ( 'NONE',  ( 2.000000000000000000, 0.000000000000000000, 0.000000000000000000 ) ) ;
#12329=VERTEX_POINT ( 'NONE', #8555 ) ;
#12337=AXIS2_PLACEMENT_3D ( 'NONE', #4568, #8147, #5681 ) ;
#12430=CIRCLE ( 'NONE', #9935, 2.749999999999999112 ) ;
#12447=ORIENTED_EDGE ( 'NONE', *, *, #12648, .T. ) ;
#12461=VERTEX_POINT ( 'NONE', #2706 ) ;
#12478=VECTOR ( 'NONE', #10611, 1000.000000000000000 ) ;
#12484=EDGE_CURVE ( 'NONE', #7800, #12769, #11158, .T. ) ;
#12540=CARTESIAN_POINT ( 'NONE',  ( 2.000000000000000000, -3.175426480542940411, 0.000000000000000000 ) ) ;
#12543=CARTESIAN_POINT ( 'NONE',  ( 2.000000000000000000, 1.587713240271468207, -2.750000000000000000 ) ) ;
#12579=LINE ( 'NONE', #10385, #2936 ) ;
#12582=AXIS2_PLACEMENT_3D ( 'NONE', #12670, #6701, #13943 ) ;
#12604=B_SPLINE_CURVE_WITH_KNOTS ( 'NONE', 3,
 ( #10851, #550, #630, #11233, #1824, #10208 ),
 .UNSPECIFIED., .F., .F.,
 ( 4, 2, 4 ),
 ( 0.001606744326298690335, 0.002406996759593249199, 0.003207249192887807847 ),
 .UNSPECIFIED. ) ;
#12635=ORIENTED_EDGE ( 'NONE', *, *, #2924, .T. ) ;
#12648=EDGE_CURVE ( 'NONE', #12769, #10711, #9990, .T. ) ;
#12670=CARTESIAN_POINT ( 'NONE',  ( 2.000000000000000000, 1.587713240271468207, -2.750000000000000000 ) ) ;
#12683=CONICAL_SURFACE ( 'NONE', #12180, 1.219500000000000028, 0.7853981633974552734 ) ;
#12685=LINE ( 'NONE', #4317, #5452 ) ;
#12726=ORIENTED_EDGE ( 'NONE', *, *, #5142, .F. ) ;
#12769=VERTEX_POINT ( 'NONE', #519 ) ;
#12792=ORIENTED_EDGE ( 'NONE', *, *, #13104, .F. ) ;
#12796=CIRCLE ( 'NONE', #10801, 1.499999999999999778 ) ;
#12820=EDGE_CURVE ( 'NONE', #6134, #9639, #12685, .T. ) ;
#12882=PRODUCT_DEFINITION ( 'UNKNOWN', '', #188, #6482 ) ;
#12985=ADVANCED_FACE ( 'NONE', ( #5902 ), #12683, .T. ) ;
#12989=ORIENTED_EDGE ( 'NONE', *, *, #5482, .T. ) ;
#12992=DIRECTION ( 'NONE',  ( 0.000000000000000000, 0.000000000000000000, -1.000000000000000000 ) ) ;
#13045=PRESENTATION_STYLE_ASSIGNMENT (( #1207 ) ) ;
#13075=CARTESIAN_POINT ( 'NONE',  ( 0.2456200930618588907, -1.587713240271461546, 2.750000000000000000 ) ) ;
#13104=EDGE_CURVE ( 'NONE', #7691, #13181, #9251, .T. ) ;
#13149=AXIS2_PLACEMENT_3D ( 'NONE', #1387, #9704, #6076 ) ;
#13163=CARTESIAN_POINT ( 'NONE',  ( 0.02377086945486034386, 0.5410735902665446684, 2.750000000000001332 ) ) ;
#13178=ORIENTED_EDGE ( 'NONE', *, *, #5178, .T. ) ;
#13181=VERTEX_POINT ( 'NONE', #5747 ) ;
#13187=ORIENTED_EDGE ( 'NONE', *, *, #14470, .F. ) ;
#13192=ORIENTED_EDGE ( 'NONE', *, *, #13104, .T. ) ;
#13238=DIRECTION ( 'NONE',  ( -1.000000000000000000, -0.000000000000000000, -0.000000000000000000 ) ) ;
#13243=DIRECTION ( 'NONE',  ( 0.000000000000000000, 0.000000000000000000, 1.000000000000000000 ) ) ;
#13311=CARTESIAN_POINT ( 'NONE',  ( 0.2456200930618607225, -3.175426480542939967, 2.004439700231694701E-16 ) ) ;
#13355=CARTESIAN_POINT ( 'NONE',  ( 0.2456200930618607225, -3.175426480542939967, 2.004439700231694701E-16 ) ) ;
#13365=ORIENTED_EDGE ( 'NONE', *, *, #3762, .T. ) ;
#13395=ORIENTED_EDGE ( 'NONE', *, *, #12820, .F. ) ;
#13399=LINE ( 'NONE', #4965, #11399 ) ;
#13405=CARTESIAN_POINT ( 'NONE',  ( 2.000000000000000000, 1.836970198721029688E-16, -1.499999999999999778 ) ) ;
#13515=CARTESIAN_POINT ( 'NONE',  ( 0.000000000000000000, 0.000000000000000000, 1.499999999999999778 ) ) ;
#13542=ORIENTED_EDGE ( 'NONE', *, *, #10269, .T. ) ;
#13553=EDGE_CURVE ( 'NONE', #8109, #6130, #1546, .T. ) ;
#13558=CARTESIAN_POINT ( 'NONE',  ( 7.572474548453445031E-16, 0.2688604483138313794, -2.750000000000000888 ) ) ;
#13578=CONICAL_SURFACE ( 'NONE', #14584, 2.749999999999999112, 1.047197551196600296 ) ;
#13594=CARTESIAN_POINT ( 'NONE',  ( 0.000000000000000000, 2.381569860407203532, -1.375000000000002665 ) ) ;
#13603=ADVANCED_FACE ( 'NONE', ( #1802 ), #11364, .F. ) ;
#13611=FACE_OUTER_BOUND ( 'NONE', #2713, .T. ) ;
#13650=PLANE ( 'NONE',  #14932 ) ;
#13689=VECTOR ( 'NONE', #5669, 1000.000000000000114 ) ;
#13691=DIRECTION ( 'NONE',  ( 0.000000000000000000, 0.8660254037844375974, -0.5000000000000018874 ) ) ;
#13717=ORIENTED_EDGE ( 'NONE', *, *, #5674, .F. ) ;
#13730=CARTESIAN_POINT ( 'NONE',  ( 2.000000000000000000, -1.587713240271461546, 2.750000000000000000 ) ) ;
#13739=ORIENTED_EDGE ( 'NONE', *, *, #7587, .F. ) ;
#13740=DIRECTION ( 'NONE',  ( -1.000000000000000000, -0.000000000000000000, -0.000000000000000000 ) ) ;
#13753=EDGE_CURVE ( 'NONE', #3709, #11977, #12796, .T. ) ;
#13773=CARTESIAN_POINT ( 'NONE',  ( 0.1085346982764772705, -1.064859738961390079, 2.750000000000000444 ) ) ;
#13783=CARTESIAN_POINT ( 'NONE',  ( 0.2456200930618618050, 1.587713240271470427, 2.750000000000000888 ) ) ;
#13833=DIRECTION ( 'NONE',  ( -1.000000000000000000, -0.000000000000000000, -0.000000000000000000 ) ) ;
#13943=DIRECTION ( 'NONE',  ( 0.000000000000000000, -0.5000000000000012212, -0.8660254037844380415 ) ) ;
#13945=ORIENTED_EDGE ( 'NONE', *, *, #5482, .F. ) ;
#14027=AXIS2_PLACEMENT_3D ( 'NONE', #9872, #11046, #11204 ) ;
#14100=AXIS2_PLACEMENT_3D ( 'NONE', #503, #5344, #8909 ) ;
#14133=CIRCLE ( 'NONE', #1272, 1.500000000000000000 ) ;
#14144=EDGE_CURVE ( 'NONE', #4933, #5606, #15236, .T. ) ;
#14149=ORIENTED_EDGE ( 'NONE', *, *, #6717, .F. ) ;
#14153=ORIENTED_EDGE ( 'NONE', *, *, #10427, .F. ) ;
#14159=CARTESIAN_POINT ( 'NONE',  ( 0.000000000000000000, 7.511572993685799101E-16, -2.750000000000000444 ) ) ;
#14179=CARTESIAN_POINT ( 'NONE',  ( 21.99999999999999289, 0.000000000000000000, 0.000000000000000000 ) ) ;
#14197=AXIS2_PLACEMENT_3D ( 'NONE', #7817, #7657, #6473 ) ;
#14200=ORIENTED_EDGE ( 'NONE', *, *, #10489, .F. ) ;
#14272=FACE_OUTER_BOUND ( 'NONE', #6735, .T. ) ;
#14298=DIRECTION ( 'NONE',  ( 0.000000000000000000, -2.731481088613017720E-16, 1.000000000000000000 ) ) ;
#14337=DIRECTION ( 'NONE',  ( -1.000000000000000000, -0.000000000000000000, 0.000000000000000000 ) ) ;
#14349=DIRECTION ( 'NONE',  ( 1.000000000000000000, 0.000000000000000000, -0.000000000000000000 ) ) ;
#14403=VECTOR ( 'NONE', #1090, 1000.000000000000000 ) ;
#14425=EDGE_CURVE ( 'NONE', #12461, #7800, #3485, .T. ) ;
#14443=CARTESIAN_POINT ( 'NONE',  ( 0.000000000000000000, 0.000000000000000000, 0.000000000000000000 ) ) ;
#14448=DIRECTION ( 'NONE',  ( 1.000000000000000000, 0.000000000000000000, 0.000000000000000000 ) ) ;
#14470=EDGE_CURVE ( 'NONE', #12329, #7691, #6533, .T. ) ;
#14502=CYLINDRICAL_SURFACE ( 'NONE', #11425, 1.499999999999999778 ) ;
#14563=B_SPLINE_CURVE_WITH_KNOTS ( 'NONE', 3,
 ( #3935, #12222, #11131, #127 ),
 .UNSPECIFIED., .F., .F.,
 ( 4, 4 ),
 ( 2.380742993382810214E-07, 0.001606744326298690335 ),
 .UNSPECIFIED. ) ;
#14580=PLANE ( 'NONE',  #5213 ) ;
#14584=AXIS2_PLACEMENT_3D ( 'NONE', #10897, #3543, #7348 ) ;
#14679=CARTESIAN_POINT ( 'NONE',  ( 2.000000000000000000, 1.587713240271468207, -2.750000000000000000 ) ) ;
#14699=CARTESIAN_POINT ( 'NONE',  ( 0.2456200930617507272, -1.587713240271640958, -2.750000000000000888 ) ) ;
#14914=CARTESIAN_POINT ( 'NONE',  ( 2.000000000000000000, 1.587713240271470427, 2.750000000000000888 ) ) ;
#14932=AXIS2_PLACEMENT_3D ( 'NONE', #14914, #3881, #4106 ) ;
#14956=DIRECTION ( 'NONE',  ( 0.000000000000000000, 0.000000000000000000, -1.000000000000000000 ) ) ;
#14963=CARTESIAN_POINT ( 'NONE',  ( 0.000000000000000000, -2.381569860407202643, 1.375000000000004663 ) ) ;
#15025=ADVANCED_FACE ( 'NONE', ( #723 ), #3423, .F. ) ;
#15075=EDGE_LOOP ( 'NONE', ( #13192, #5135, #4178 ) ) ;
#15104=CARTESIAN_POINT ( 'NONE',  ( 0.2456200930618588907, -1.587713240271461546, 2.750000000000000000 ) ) ;
#15135=ORIENTED_EDGE ( 'NONE', *, *, #2424, .T. ) ;
#15207=EDGE_CURVE ( 'NONE', #11977, #3709, #8813, .T. ) ;
#15215=EDGE_LOOP ( 'NONE', ( #2011, #12989, #6032 ) ) ;
#15236=B_SPLINE_CURVE_WITH_KNOTS ( 'NONE', 3,
 ( #4717, #3459, #924, #9539, #7026, #13075 ),
 .UNSPECIFIED., .F., .F.,
 ( 4, 2, 4 ),
 ( 0.001606744326298693154, 0.002406996759593252669, 0.003207249192887813051 ),
 .UNSPECIFIED. ) ;
#15322=EDGE_CURVE ( 'NONE', #12236, #9639, #12604, .T. ) ;
#15328=ORIENTED_EDGE ( 'NONE', *, *, #15207, .F. ) ;
#15356=DIRECTION ( 'NONE',  ( 0.000000000000000000, 0.000000000000000000, 1.000000000000000000 ) ) ;
#15368=VERTEX_POINT ( 'NONE', #10278 ) ;
#15411=CARTESIAN_POINT ( 'NONE',  ( 0.02351960456806117053, 2.650883748492876446, 0.9085346626517036839 ) ) ;
#15424=CONICAL_SURFACE ( 'NONE', #4598, 2.749999999999999112, 1.047197551196600296 ) ;
#15432=DIRECTION ( 'NONE',  ( 0.000000000000000000, 0.000000000000000000, 1.000000000000000000 ) ) ;
#15543=DIRECTION ( 'NONE',  ( 0.000000000000000000, 0.000000000000000000, -1.000000000000000000 ) ) ;
#15567=( NAMED_UNIT ( * ) PLANE_ANGLE_UNIT ( ) SI_UNIT ( $, .RADIAN. ) );
ENDSEC;
END-ISO-10303-21;
